ISO-10303-21;
HEADER;
/* Generated by software containing ST-Developer
 * from STEP Tools, Inc. (www.steptools.com) 
 */

FILE_DESCRIPTION(
/* description */ (''),
/* implementation_level */ '2;1');

FILE_NAME(
/* name */ '12_Circlip_DIN_471_-_25.step',
/* time_stamp */ '2026-10-26T04:15:57-07:00',
/* author */ (''),
/* organization */ (''),
/* preprocessor_version */ 'ST-DEVELOPER v20.2',
/* originating_system */ 'Autodesk Translation Framework v15.15.0.0',
/* authorisation */ '');

FILE_SCHEMA (('AUTOMOTIVE_DESIGN { 1 0 10303 214 3 1 1 }'));
ENDSEC;

DATA;
#10=MECHANICAL_DESIGN_GEOMETRIC_PRESENTATION_REPRESENTATION('',(#463),#55737);
#330=ELLIPSE('',#29202,16.8998520703585,11.95);
#331=ELLIPSE('',#29207,16.8998520703585,11.95);
#332=ELLIPSE('',#29211,16.8998520703585,11.95);
#333=ELLIPSE('',#29213,16.8998520703585,11.95);
#379=CONICAL_SURFACE('',#29203,15.9,0.78539816339744);
#380=CONICAL_SURFACE('',#29214,15.9,0.78539816339744);
#423=SHAPE_REPRESENTATION_RELATIONSHIP('SRR','None',#55832,#443);
#443=ADVANCED_BREP_SHAPE_REPRESENTATION('',(#483),#55728);
#463=STYLED_ITEM('',(#55991),#483);
#483=MANIFOLD_SOLID_BREP('Body1',#27232);
#1397=PLANE('',#29201);
#1398=PLANE('',#29206);
#1399=PLANE('',#29208);
#1400=PLANE('',#29210);
#1401=PLANE('',#29212);
#1402=PLANE('',#29217);
#1403=PLANE('',#29219);
#1404=PLANE('',#29222);
#3340=LINE('',#45283,#5711);
#3341=LINE('',#45287,#5712);
#3342=LINE('',#45303,#5713);
#3343=LINE('',#45306,#5714);
#3344=LINE('',#45312,#5715);
#3345=LINE('',#45316,#5716);
#3346=LINE('',#45324,#5717);
#3347=LINE('',#45328,#5718);
#3348=LINE('',#45339,#5719);
#3349=LINE('',#45340,#5720);
#3350=LINE('',#45342,#5721);
#3351=LINE('',#45344,#5722);
#5711=VECTOR('',#35038,10.);
#5712=VECTOR('',#35041,10.);
#5713=VECTOR('',#35050,10.);
#5714=VECTOR('',#35053,10.);
#5715=VECTOR('',#35060,10.);
#5716=VECTOR('',#35063,10.);
#5717=VECTOR('',#35066,10.);
#5718=VECTOR('',#35069,10.);
#5719=VECTOR('',#35082,10.);
#5720=VECTOR('',#35083,10.);
#5721=VECTOR('',#35086,10.);
#5722=VECTOR('',#35089,10.);
#6694=CYLINDRICAL_SURFACE('',#29220,16.);
#6695=CYLINDRICAL_SURFACE('',#29221,11.95);
#7856=FACE_OUTER_BOUND('',#9525,.T.);
#7857=FACE_OUTER_BOUND('',#9526,.T.);
#7858=FACE_OUTER_BOUND('',#9527,.T.);
#7859=FACE_OUTER_BOUND('',#9528,.T.);
#7860=FACE_OUTER_BOUND('',#9529,.T.);
#7861=FACE_OUTER_BOUND('',#9530,.T.);
#7862=FACE_OUTER_BOUND('',#9531,.T.);
#7863=FACE_OUTER_BOUND('',#9532,.T.);
#7864=FACE_OUTER_BOUND('',#9533,.T.);
#7865=FACE_OUTER_BOUND('',#9534,.T.);
#7866=FACE_OUTER_BOUND('',#9535,.T.);
#7867=FACE_OUTER_BOUND('',#9536,.T.);
#9525=EDGE_LOOP('',(#23006,#23007,#23008,#23009));
#9526=EDGE_LOOP('',(#23010,#23011,#23012,#23013));
#9527=EDGE_LOOP('',(#23014,#23015,#23016,#23017));
#9528=EDGE_LOOP('',(#23018,#23019,#23020,#23021));
#9529=EDGE_LOOP('',(#23022,#23023,#23024,#23025));
#9530=EDGE_LOOP('',(#23026,#23027,#23028,#23029));
#9531=EDGE_LOOP('',(#23030,#23031,#23032,#23033));
#9532=EDGE_LOOP('',(#23034,#23035,#23036,#23037));
#9533=EDGE_LOOP('',(#23038,#23039,#23040,#23041));
#9534=EDGE_LOOP('',(#23042,#23043,#23044,#23045));
#9535=EDGE_LOOP('',(#23046,#23047,#23048,#23049,#23050,#23051,#23052,#23053));
#9536=EDGE_LOOP('',(#23054,#23055,#23056,#23057));
#10782=CIRCLE('',#29204,15.8);
#10783=CIRCLE('',#29205,16.);
#10784=CIRCLE('',#29209,11.95);
#10785=CIRCLE('',#29215,16.);
#10786=CIRCLE('',#29216,15.8);
#10787=CIRCLE('',#29218,11.95);
#11194=B_SPLINE_CURVE_WITH_KNOTS('',3,(#45288,#45289,#45290,#45291),
 .UNSPECIFIED.,.F.,.F.,(4,4),(0.,0.0373327877210394),.UNSPECIFIED.);
#11195=B_SPLINE_CURVE_WITH_KNOTS('',3,(#45296,#45297,#45298,#45299),
 .UNSPECIFIED.,.F.,.F.,(4,4),(0.,0.0373327877209389),.UNSPECIFIED.);
#11196=B_SPLINE_CURVE_WITH_KNOTS('',3,(#45317,#45318,#45319,#45320),
 .UNSPECIFIED.,.F.,.F.,(4,4),(0.,0.0373327852068557),.UNSPECIFIED.);
#11197=B_SPLINE_CURVE_WITH_KNOTS('',3,(#45329,#45330,#45331,#45332),
 .UNSPECIFIED.,.F.,.F.,(4,4),(0.,0.0373327877209165),.UNSPECIFIED.);
#13092=VERTEX_POINT('',#45281);
#13093=VERTEX_POINT('',#45282);
#13094=VERTEX_POINT('',#45284);
#13095=VERTEX_POINT('',#45286);
#13096=VERTEX_POINT('',#45293);
#13097=VERTEX_POINT('',#45295);
#13098=VERTEX_POINT('',#45302);
#13099=VERTEX_POINT('',#45304);
#13100=VERTEX_POINT('',#45310);
#13101=VERTEX_POINT('',#45311);
#13102=VERTEX_POINT('',#45313);
#13103=VERTEX_POINT('',#45315);
#13104=VERTEX_POINT('',#45322);
#13105=VERTEX_POINT('',#45323);
#13106=VERTEX_POINT('',#45325);
#13107=VERTEX_POINT('',#45327);
#16507=EDGE_CURVE('',#13092,#13093,#3340,.T.);
#16508=EDGE_CURVE('',#13093,#13094,#330,.T.);
#16509=EDGE_CURVE('',#13094,#13095,#3341,.T.);
#16510=EDGE_CURVE('',#13095,#13092,#11194,.T.);
#16511=EDGE_CURVE('',#13095,#13096,#10782,.T.);
#16512=EDGE_CURVE('',#13096,#13097,#11195,.T.);
#16513=EDGE_CURVE('',#13097,#13092,#10783,.T.);
#16514=EDGE_CURVE('',#13096,#13098,#3342,.T.);
#16515=EDGE_CURVE('',#13098,#13099,#331,.T.);
#16516=EDGE_CURVE('',#13099,#13097,#3343,.T.);
#16517=EDGE_CURVE('',#13094,#13098,#10784,.T.);
#16518=EDGE_CURVE('',#13100,#13101,#3344,.T.);
#16519=EDGE_CURVE('',#13101,#13102,#332,.T.);
#16520=EDGE_CURVE('',#13102,#13103,#3345,.T.);
#16521=EDGE_CURVE('',#13103,#13100,#11196,.T.);
#16522=EDGE_CURVE('',#13104,#13105,#3346,.T.);
#16523=EDGE_CURVE('',#13105,#13106,#333,.T.);
#16524=EDGE_CURVE('',#13106,#13107,#3347,.T.);
#16525=EDGE_CURVE('',#13107,#13104,#11197,.T.);
#16526=EDGE_CURVE('',#13103,#13104,#10785,.T.);
#16527=EDGE_CURVE('',#13107,#13100,#10786,.T.);
#16528=EDGE_CURVE('',#13106,#13101,#10787,.T.);
#16529=EDGE_CURVE('',#13105,#13099,#3348,.T.);
#16530=EDGE_CURVE('',#13104,#13097,#3349,.T.);
#16531=EDGE_CURVE('',#13103,#13092,#3350,.T.);
#16532=EDGE_CURVE('',#13102,#13093,#3351,.T.);
#23006=ORIENTED_EDGE('',*,*,#16507,.T.);
#23007=ORIENTED_EDGE('',*,*,#16508,.T.);
#23008=ORIENTED_EDGE('',*,*,#16509,.T.);
#23009=ORIENTED_EDGE('',*,*,#16510,.T.);
#23010=ORIENTED_EDGE('',*,*,#16511,.T.);
#23011=ORIENTED_EDGE('',*,*,#16512,.T.);
#23012=ORIENTED_EDGE('',*,*,#16513,.T.);
#23013=ORIENTED_EDGE('',*,*,#16510,.F.);
#23014=ORIENTED_EDGE('',*,*,#16514,.T.);
#23015=ORIENTED_EDGE('',*,*,#16515,.T.);
#23016=ORIENTED_EDGE('',*,*,#16516,.T.);
#23017=ORIENTED_EDGE('',*,*,#16512,.F.);
#23018=ORIENTED_EDGE('',*,*,#16514,.F.);
#23019=ORIENTED_EDGE('',*,*,#16511,.F.);
#23020=ORIENTED_EDGE('',*,*,#16509,.F.);
#23021=ORIENTED_EDGE('',*,*,#16517,.T.);
#23022=ORIENTED_EDGE('',*,*,#16518,.T.);
#23023=ORIENTED_EDGE('',*,*,#16519,.T.);
#23024=ORIENTED_EDGE('',*,*,#16520,.T.);
#23025=ORIENTED_EDGE('',*,*,#16521,.T.);
#23026=ORIENTED_EDGE('',*,*,#16522,.T.);
#23027=ORIENTED_EDGE('',*,*,#16523,.T.);
#23028=ORIENTED_EDGE('',*,*,#16524,.T.);
#23029=ORIENTED_EDGE('',*,*,#16525,.T.);
#23030=ORIENTED_EDGE('',*,*,#16526,.T.);
#23031=ORIENTED_EDGE('',*,*,#16525,.F.);
#23032=ORIENTED_EDGE('',*,*,#16527,.T.);
#23033=ORIENTED_EDGE('',*,*,#16521,.F.);
#23034=ORIENTED_EDGE('',*,*,#16518,.F.);
#23035=ORIENTED_EDGE('',*,*,#16527,.F.);
#23036=ORIENTED_EDGE('',*,*,#16524,.F.);
#23037=ORIENTED_EDGE('',*,*,#16528,.T.);
#23038=ORIENTED_EDGE('',*,*,#16516,.F.);
#23039=ORIENTED_EDGE('',*,*,#16529,.F.);
#23040=ORIENTED_EDGE('',*,*,#16522,.F.);
#23041=ORIENTED_EDGE('',*,*,#16530,.T.);
#23042=ORIENTED_EDGE('',*,*,#16513,.F.);
#23043=ORIENTED_EDGE('',*,*,#16530,.F.);
#23044=ORIENTED_EDGE('',*,*,#16526,.F.);
#23045=ORIENTED_EDGE('',*,*,#16531,.T.);
#23046=ORIENTED_EDGE('',*,*,#16515,.F.);
#23047=ORIENTED_EDGE('',*,*,#16517,.F.);
#23048=ORIENTED_EDGE('',*,*,#16508,.F.);
#23049=ORIENTED_EDGE('',*,*,#16532,.F.);
#23050=ORIENTED_EDGE('',*,*,#16519,.F.);
#23051=ORIENTED_EDGE('',*,*,#16528,.F.);
#23052=ORIENTED_EDGE('',*,*,#16523,.F.);
#23053=ORIENTED_EDGE('',*,*,#16529,.T.);
#23054=ORIENTED_EDGE('',*,*,#16507,.F.);
#23055=ORIENTED_EDGE('',*,*,#16531,.F.);
#23056=ORIENTED_EDGE('',*,*,#16520,.F.);
#23057=ORIENTED_EDGE('',*,*,#16532,.T.);
#26680=ADVANCED_FACE('',(#7856),#1397,.T.);
#26681=ADVANCED_FACE('',(#7857),#379,.T.);
#26682=ADVANCED_FACE('',(#7858),#1398,.T.);
#26683=ADVANCED_FACE('',(#7859),#1399,.T.);
#26684=ADVANCED_FACE('',(#7860),#1400,.T.);
#26685=ADVANCED_FACE('',(#7861),#1401,.T.);
#26686=ADVANCED_FACE('',(#7862),#380,.T.);
#26687=ADVANCED_FACE('',(#7863),#1402,.F.);
#26688=ADVANCED_FACE('',(#7864),#1403,.T.);
#26689=ADVANCED_FACE('',(#7865),#6694,.T.);
#26690=ADVANCED_FACE('',(#7866),#6695,.F.);
#26691=ADVANCED_FACE('',(#7867),#1404,.T.);
#27232=CLOSED_SHELL('',(#26680,#26681,#26682,#26683,#26684,#26685,#26686,
#26687,#26688,#26689,#26690,#26691));
#29200=AXIS2_PLACEMENT_3D('',#45279,#35034,#35035);
#29201=AXIS2_PLACEMENT_3D('',#45280,#35036,#35037);
#29202=AXIS2_PLACEMENT_3D('',#45285,#35039,#35040);
#29203=AXIS2_PLACEMENT_3D('',#45292,#35042,#35043);
#29204=AXIS2_PLACEMENT_3D('',#45294,#35044,#35045);
#29205=AXIS2_PLACEMENT_3D('',#45300,#35046,#35047);
#29206=AXIS2_PLACEMENT_3D('',#45301,#35048,#35049);
#29207=AXIS2_PLACEMENT_3D('',#45305,#35051,#35052);
#29208=AXIS2_PLACEMENT_3D('',#45307,#35054,#35055);
#29209=AXIS2_PLACEMENT_3D('',#45308,#35056,#35057);
#29210=AXIS2_PLACEMENT_3D('',#45309,#35058,#35059);
#29211=AXIS2_PLACEMENT_3D('',#45314,#35061,#35062);
#29212=AXIS2_PLACEMENT_3D('',#45321,#35064,#35065);
#29213=AXIS2_PLACEMENT_3D('',#45326,#35067,#35068);
#29214=AXIS2_PLACEMENT_3D('',#45333,#35070,#35071);
#29215=AXIS2_PLACEMENT_3D('',#45334,#35072,#35073);
#29216=AXIS2_PLACEMENT_3D('',#45335,#35074,#35075);
#29217=AXIS2_PLACEMENT_3D('',#45336,#35076,#35077);
#29218=AXIS2_PLACEMENT_3D('',#45337,#35078,#35079);
#29219=AXIS2_PLACEMENT_3D('',#45338,#35080,#35081);
#29220=AXIS2_PLACEMENT_3D('',#45341,#35084,#35085);
#29221=AXIS2_PLACEMENT_3D('',#45343,#35087,#35088);
#29222=AXIS2_PLACEMENT_3D('',#45345,#35090,#35091);
#35034=DIRECTION('axis',(0.,0.,1.));
#35035=DIRECTION('refdir',(1.,0.,0.));
#35036=DIRECTION('center_axis',(0.707106781186548,-0.707106781186547,0.));
#35037=DIRECTION('ref_axis',(0.,0.,-1.));
#35038=DIRECTION('',(0.,0.,-1.));
#35039=DIRECTION('center_axis',(-0.707106781186548,0.707106781186547,0.));
#35040=DIRECTION('ref_axis',(-0.707106781186547,-0.707106781186548,6.56942451332124E-17));
#35041=DIRECTION('',(0.,0.,1.));
#35042=DIRECTION('center_axis',(-1.,0.,0.));
#35043=DIRECTION('ref_axis',(0.,0.1875,-0.982264602843857));
#35044=DIRECTION('center_axis',(-1.,0.,0.));
#35045=DIRECTION('ref_axis',(0.,0.1875,-0.982264602843857));
#35046=DIRECTION('center_axis',(1.,0.,0.));
#35047=DIRECTION('ref_axis',(0.,0.1875,-0.982264602843857));
#35048=DIRECTION('center_axis',(0.707106781186548,0.707106781186547,0.));
#35049=DIRECTION('ref_axis',(0.,0.,-1.));
#35050=DIRECTION('',(0.,0.,-1.));
#35051=DIRECTION('center_axis',(-0.707106781186548,-0.707106781186547,0.));
#35052=DIRECTION('ref_axis',(0.707106781186547,-0.707106781186548,6.56942451332124E-17));
#35053=DIRECTION('',(0.,0.,1.));
#35054=DIRECTION('center_axis',(1.,0.,0.));
#35055=DIRECTION('ref_axis',(0.,0.,-1.));
#35056=DIRECTION('center_axis',(-1.,0.,0.));
#35057=DIRECTION('ref_axis',(0.,-0.251046025104602,0.967975151168241));
#35058=DIRECTION('center_axis',(-0.707106781186548,-0.707106781186547,0.));
#35059=DIRECTION('ref_axis',(0.,0.,1.));
#35060=DIRECTION('',(0.,0.,-1.));
#35061=DIRECTION('center_axis',(0.707106781186548,0.707106781186547,0.));
#35062=DIRECTION('ref_axis',(0.707106781186547,-0.707106781186548,6.56942451332124E-17));
#35063=DIRECTION('',(0.,0.,1.));
#35064=DIRECTION('center_axis',(-0.707106781186548,0.707106781186547,0.));
#35065=DIRECTION('ref_axis',(0.,0.,1.));
#35066=DIRECTION('',(0.,0.,-1.));
#35067=DIRECTION('center_axis',(0.707106781186548,-0.707106781186547,0.));
#35068=DIRECTION('ref_axis',(-0.707106781186547,-0.707106781186548,6.56942451332124E-17));
#35069=DIRECTION('',(0.,0.,1.));
#35070=DIRECTION('center_axis',(1.,0.,0.));
#35071=DIRECTION('ref_axis',(0.,0.1875,-0.982264602843857));
#35072=DIRECTION('center_axis',(-1.,0.,0.));
#35073=DIRECTION('ref_axis',(0.,0.1875,-0.982264602843857));
#35074=DIRECTION('center_axis',(1.,0.,0.));
#35075=DIRECTION('ref_axis',(0.,0.1875,-0.982264602843857));
#35076=DIRECTION('center_axis',(1.,0.,0.));
#35077=DIRECTION('ref_axis',(0.,0.,-1.));
#35078=DIRECTION('center_axis',(1.,0.,0.));
#35079=DIRECTION('ref_axis',(0.,-0.251046025104602,0.967975151168241));
#35080=DIRECTION('center_axis',(0.,1.,0.));
#35081=DIRECTION('ref_axis',(0.,0.,1.));
#35082=DIRECTION('',(1.,0.,0.));
#35083=DIRECTION('',(1.,0.,0.));
#35084=DIRECTION('center_axis',(1.,0.,0.));
#35085=DIRECTION('ref_axis',(0.,-2.42861286636753E-16,-1.));
#35086=DIRECTION('',(1.,0.,0.));
#35087=DIRECTION('center_axis',(1.,0.,0.));
#35088=DIRECTION('ref_axis',(0.,9.29056924372516E-17,-1.));
#35089=DIRECTION('',(1.,0.,0.));
#35090=DIRECTION('center_axis',(0.,-1.,0.));
#35091=DIRECTION('ref_axis',(0.,0.,-1.));
#45279=CARTESIAN_POINT('',(0.,0.,0.));
#45280=CARTESIAN_POINT('Origin',(1.1,3.1,7.78717523412628));
#45281=CARTESIAN_POINT('',(1.,3.,15.7162336455017));
#45282=CARTESIAN_POINT('',(1.,3.,11.5673030564605));
#45283=CARTESIAN_POINT('',(1.,3.,7.78717523412628));
#45284=CARTESIAN_POINT('',(1.2,3.2,11.5135789396695));
#45285=CARTESIAN_POINT('Origin',(-2.,0.,3.12250225675825E-16));
#45286=CARTESIAN_POINT('',(1.2,3.2,15.4725563498732));
#45287=CARTESIAN_POINT('',(1.2,3.2,7.78717523412628));
#45288=CARTESIAN_POINT('Ctrl Pts',(1.2,3.2,15.4725563498732));
#45289=CARTESIAN_POINT('Ctrl Pts',(1.13355790711216,3.13355790711216,15.554145955128));
#45290=CARTESIAN_POINT('Ctrl Pts',(1.06688589706653,3.06688589706653,15.6353725388951));
#45291=CARTESIAN_POINT('Ctrl Pts',(1.,3.,15.7162336455017));
#45292=CARTESIAN_POINT('Origin',(1.1,0.,-1.90819582357449E-16));
#45293=CARTESIAN_POINT('',(1.2,-3.2,15.4725563498732));
#45294=CARTESIAN_POINT('Origin',(1.2,0.,-1.90819582357449E-16));
#45295=CARTESIAN_POINT('',(1.,-3.,15.7162336455017));
#45296=CARTESIAN_POINT('Ctrl Pts',(1.2,-3.2,15.4725563498732));
#45297=CARTESIAN_POINT('Ctrl Pts',(1.13355790711234,-3.13355790711234,15.5541459551277));
#45298=CARTESIAN_POINT('Ctrl Pts',(1.06688589706689,-3.0668858970669,15.6353725388946));
#45299=CARTESIAN_POINT('Ctrl Pts',(1.,-3.,15.7162336455017));
#45300=CARTESIAN_POINT('Origin',(1.,0.,-1.90819582357449E-16));
#45301=CARTESIAN_POINT('Origin',(1.1,-3.1,5.71270993960567));
#45302=CARTESIAN_POINT('',(1.2,-3.2,11.5135789396695));
#45303=CARTESIAN_POINT('',(1.2,-3.2,5.71270993960567));
#45304=CARTESIAN_POINT('',(1.,-3.,11.5673030564605));
#45305=CARTESIAN_POINT('Origin',(-2.,0.,3.12250225675825E-16));
#45306=CARTESIAN_POINT('',(1.,-3.,5.71270993960567));
#45307=CARTESIAN_POINT('Origin',(1.2,0.,-0.141883177249145));
#45308=CARTESIAN_POINT('Origin',(1.2,0.,3.12250225675825E-16));
#45309=CARTESIAN_POINT('Origin',(0.1,3.1,7.78717523412628));
#45310=CARTESIAN_POINT('',(0.,3.2,15.4725563498732));
#45311=CARTESIAN_POINT('',(0.,3.2,11.5135789396695));
#45312=CARTESIAN_POINT('',(0.,3.2,7.78717523412628));
#45313=CARTESIAN_POINT('',(0.2,3.,11.5673030564605));
#45314=CARTESIAN_POINT('Origin',(3.2,0.,3.12250225675825E-16));
#45315=CARTESIAN_POINT('',(0.2,3.,15.7162336455017));
#45316=CARTESIAN_POINT('',(0.2,3.,7.78717523412628));
#45317=CARTESIAN_POINT('Ctrl Pts',(0.2,3.,15.7162336455017));
#45318=CARTESIAN_POINT('Ctrl Pts',(0.133114102933436,3.06688589706656,15.635372538895));
#45319=CARTESIAN_POINT('Ctrl Pts',(0.0664420928878206,3.13355790711218,
15.5541459551279));
#45320=CARTESIAN_POINT('Ctrl Pts',(-1.96023752785379E-15,3.2,15.4725563498732));
#45321=CARTESIAN_POINT('Origin',(0.1,-3.1,5.71270993960567));
#45322=CARTESIAN_POINT('',(0.2,-3.,15.7162336455017));
#45323=CARTESIAN_POINT('',(0.2,-3.,11.5673030564605));
#45324=CARTESIAN_POINT('',(0.2,-3.,5.71270993960567));
#45325=CARTESIAN_POINT('',(0.,-3.2,11.5135789396695));
#45326=CARTESIAN_POINT('Origin',(3.2,0.,3.12250225675825E-16));
#45327=CARTESIAN_POINT('',(0.,-3.2,15.4725563498732));
#45328=CARTESIAN_POINT('',(0.,-3.2,5.71270993960567));
#45329=CARTESIAN_POINT('Ctrl Pts',(-2.94902990916057E-16,-3.2,15.4725563498732));
#45330=CARTESIAN_POINT('Ctrl Pts',(0.066442092887622,-3.13355790711238,
15.5541459551277));
#45331=CARTESIAN_POINT('Ctrl Pts',(0.133114102933025,-3.06688589706697,
15.6353725388945));
#45332=CARTESIAN_POINT('Ctrl Pts',(0.2,-3.,15.7162336455017));
#45333=CARTESIAN_POINT('Origin',(0.1,0.,-1.90819582357449E-16));
#45334=CARTESIAN_POINT('Origin',(0.2,0.,-1.90819582357449E-16));
#45335=CARTESIAN_POINT('Origin',(0.,0.,-1.90819582357449E-16));
#45336=CARTESIAN_POINT('Origin',(0.,0.,-0.141883177249145));
#45337=CARTESIAN_POINT('Origin',(0.,0.,3.12250225675825E-16));
#45338=CARTESIAN_POINT('Origin',(0.,-3.,11.5673030564605));
#45339=CARTESIAN_POINT('',(0.,-3.,11.5673030564605));
#45340=CARTESIAN_POINT('',(0.,-3.,15.7162336455017));
#45341=CARTESIAN_POINT('Origin',(0.,0.,-1.90819582357449E-16));
#45342=CARTESIAN_POINT('',(0.,3.,15.7162336455017));
#45343=CARTESIAN_POINT('Origin',(0.,0.,3.12250225675825E-16));
#45344=CARTESIAN_POINT('',(0.,3.,11.5673030564605));
#45345=CARTESIAN_POINT('Origin',(0.,3.,15.7162336455017));
#55706=UNCERTAINTY_MEASURE_WITH_UNIT(LENGTH_MEASURE(0.01),#55738,
'DISTANCE_ACCURACY_VALUE',
'Maximum model space distance between geometric entities at asserted c
onnectivities');
#55715=UNCERTAINTY_MEASURE_WITH_UNIT(LENGTH_MEASURE(0.01),#55738,
'DISTANCE_ACCURACY_VALUE',
'Maximum model space distance between geometric entities at asserted c
onnectivities');
#55728=(
GEOMETRIC_REPRESENTATION_CONTEXT(3)
GLOBAL_UNCERTAINTY_ASSIGNED_CONTEXT((#55706))
GLOBAL_UNIT_ASSIGNED_CONTEXT((#55738,#55740,#55741))
REPRESENTATION_CONTEXT('','3D')
);
#55737=(
GEOMETRIC_REPRESENTATION_CONTEXT(3)
GLOBAL_UNCERTAINTY_ASSIGNED_CONTEXT((#55715))
GLOBAL_UNIT_ASSIGNED_CONTEXT((#55738,#55740,#55741))
REPRESENTATION_CONTEXT('','3D')
);
#55738=(
LENGTH_UNIT()
NAMED_UNIT(*)
SI_UNIT(.MILLI.,.METRE.)
);
#55740=(
NAMED_UNIT(*)
PLANE_ANGLE_UNIT()
SI_UNIT($,.RADIAN.)
);
#55741=(
NAMED_UNIT(*)
SI_UNIT($,.STERADIAN.)
SOLID_ANGLE_UNIT()
);
#55754=SHAPE_DEFINITION_REPRESENTATION(#55775,#55832);
#55775=PRODUCT_DEFINITION_SHAPE('',$,#55854);
#55832=SHAPE_REPRESENTATION('',(#29200),#55728);
#55841=PRODUCT_DEFINITION_CONTEXT('part definition',#55906,'design');
#55854=PRODUCT_DEFINITION('2026-10-26-00-34-26-883',
'12_Circlip_DIN_471_-_25',#55875,#55841);
#55875=PRODUCT_DEFINITION_FORMATION('',$,#55920);
#55906=APPLICATION_CONTEXT(
'Core Data for Automotive Mechanical Design Process');
#55907=PRODUCT_CONTEXT('part definition',#55906,'mechanical');
#55920=PRODUCT('2026-10-26-00-34-26-883','12_Circlip_DIN_471_-_25',$,(#55907));
#55985=COLOUR_RGB('Grey',0.48,0.52,0.57);
#55986=FILL_AREA_STYLE_COLOUR('',#55985);
#55987=FILL_AREA_STYLE('',(#55986));
#55988=SURFACE_STYLE_FILL_AREA(#55987);
#55989=SURFACE_SIDE_STYLE('',(#55988));
#55990=SURFACE_STYLE_USAGE(.BOTH.,#55989);
#55991=PRESENTATION_STYLE_ASSIGNMENT((#55990));
ENDSEC;
END-ISO-10303-21;
